ISO-10303-21;
HEADER;
FILE_DESCRIPTION (('STEP AP214'),
    '1' );
FILE_NAME ('slotted pan head screw_bsi_BS EN ISO 1580 - M5 x 25 - 25N.step',
    '2026-10-06T08:09:25',
    ( '' ),
    ( '' ),
    'SwSTEP 2.0',
    'SolidWorks 2021',
    '' );
FILE_SCHEMA (( 'AUTOMOTIVE_DESIGN' ));
ENDSEC;

DATA;
#64=EDGE_CURVE ( 'NONE', #19657, #547, #12184, .T. ) ;
#83=PLANE ( 'NONE',  #17902 ) ;
#140=( GEOMETRIC_REPRESENTATION_CONTEXT ( 3 ) GLOBAL_UNCERTAINTY_ASSIGNED_CONTEXT ( ( #4137 ) ) GLOBAL_UNIT_ASSIGNED_CONTEXT ( ( #21562, #16354, #5447 ) ) REPRESENTATION_CONTEXT ( 'NONE', 'WORKASPACE' ) );
#205=EDGE_LOOP ( 'NONE', ( #9340, #20187 ) ) ;
#230=APPLICATION_CONTEXT ( 'automotive_design' ) ;
#407=CARTESIAN_POINT ( 'NONE',  ( 1.199999999999992628, 0.6000000000000103029, 4.543283425070376857 ) ) ;
#418=FILL_AREA_STYLE_COLOUR ( '', #5602 ) ;
#445=CIRCLE ( 'NONE', #13220, 1.500000000000000000 ) ;
#494=CARTESIAN_POINT ( 'NONE',  ( 0.02904021785398210737, -0.5999999999999895417, 3.399959840769905206 ) ) ;
#509=ORIENTED_EDGE ( 'NONE', *, *, #11857, .T. ) ;
#541=FILL_AREA_STYLE ('',( #418 ) ) ;
#547=VERTEX_POINT ( 'NONE', #23069 ) ;
#609=CARTESIAN_POINT ( 'NONE',  ( 0.8681510425101832684, -0.5999999999999895417, -4.444131413071498393 ) ) ;
#702=AXIS2_PLACEMENT_3D ( 'NONE', #5770, #9524, #20346 ) ;
#728=DIRECTION ( 'NONE',  ( 1.000000000000000000, -4.615739097524200579E-16, -1.134196829589820086E-15 ) ) ;
#747=ORIENTED_EDGE ( 'NONE', *, *, #64, .T. ) ;
#757=CARTESIAN_POINT ( 'NONE',  ( 1.200000000000006617, 0.6000000000000067502, -4.543283425070335113 ) ) ;
#772=SHAPE_REPRESENTATION_RELATIONSHIP ( 'NONE' , 'NONE' ,  #22944, #7243 ) ;
#869=DIRECTION ( 'NONE',  ( -1.134196829589822059E-15, -6.741645191078037727E-32, 1.000000000000000000 ) ) ;
#884=UNCERTAINTY_MEASURE_WITH_UNIT (LENGTH_MEASURE( 1.000000000000000082E-05 ), #16510, 'distance_accuracy_value', 'NONE');
#887=ORIENTED_EDGE ( 'NONE', *, *, #19737, .F. ) ;
#926=EDGE_CURVE ( 'NONE', #3142, #12512, #18446, .T. ) ;
#1037=ORIENTED_EDGE ( 'NONE', *, *, #12723, .F. ) ;
#1108=CIRCLE ( 'NONE', #16476, 4.749999999999981348 ) ;
#1121=CARTESIAN_POINT ( 'NONE',  ( 1.199999999999992628, 0.6000000000000137446, 4.749999999999990230 ) ) ;
#1198=ADVANCED_FACE ( 'NONE', ( #1613 ), #13026, .T. ) ;
#1207=ADVANCED_FACE ( 'NONE', ( #12547 ), #3613, .T. ) ;
#1263=COLOUR_RGB ( '', 0.31764706, 0.68627451, 0.89019608) ;
#1438=FILL_AREA_STYLE_COLOUR ( '', #1263 ) ;
#1504=LINE ( 'NONE', #8453, #19242 ) ;
#1514=DIRECTION ( 'NONE',  ( -1.000000000000000000, 4.615739097524200579E-16, 1.134196829589820086E-15 ) ) ;
#1565=CARTESIAN_POINT ( 'NONE',  ( 2.999999999999999556, -1.685411297769503192E-31, 2.499999999999990674 ) ) ;
#1613=FACE_OUTER_BOUND ( 'NONE', #15280, .T. ) ;
#1640=STYLED_ITEM ( 'NONE', ( #13684 ), #13034 ) ;
#1675=SURFACE_STYLE_USAGE ( .BOTH. , #15775 ) ;
#1737=PLANE ( 'NONE',  #20149 ) ;
#1745=DIRECTION ( 'NONE',  ( -1.135604581876758782E-15, 2.131628207280296771E-14, 1.000000000000000000 ) ) ;
#1867=CARTESIAN_POINT ( 'NONE',  ( 1.200000000000006617, 0.6000000000000067502, -4.543283425070335113 ) ) ;
#1897=DIRECTION ( 'NONE',  ( -1.000000000000000000, 4.615739097524200579E-16, 1.134196829589820086E-15 ) ) ;
#1907=EDGE_CURVE ( 'NONE', #14019, #15168, #4796, .T. ) ;
#1999=VERTEX_POINT ( 'NONE', #19644 ) ;
#2060=EDGE_CURVE ( 'NONE', #11147, #10307, #20197, .T. ) ;
#2067=VERTEX_POINT ( 'NONE', #13046 ) ;
#2146=ORIENTED_EDGE ( 'NONE', *, *, #6980, .T. ) ;
#2158=CARTESIAN_POINT ( 'NONE',  ( 0.000000000000000000, 0.000000000000000000, 0.000000000000000000 ) ) ;
#2270=ORIENTED_EDGE ( 'NONE', *, *, #13585, .T. ) ;
#2290=( NAMED_UNIT ( * ) SI_UNIT ( $, .STERADIAN. ) SOLID_ANGLE_UNIT ( ) );
#2327=DIRECTION ( 'NONE',  ( -1.134196829589822256E-15, -2.220446049250322449E-16, 1.000000000000000000 ) ) ;
#2362=CARTESIAN_POINT ( 'NONE',  ( 0.2262162651715079187, -0.5999999999999898748, -3.877538419241197243 ) ) ;
#2439=EDGE_CURVE ( 'NONE', #12159, #20325, #5029, .T. ) ;
#2447=CARTESIAN_POINT ( 'NONE',  ( 1.200000000000006617, -0.5999999999999894307, -4.749999999999948486 ) ) ;
#2496=ORIENTED_EDGE ( 'NONE', *, *, #11857, .F. ) ;
#2667=CARTESIAN_POINT ( 'NONE',  ( 3.000000000000002665, 0.000000000000000000, 0.000000000000000000 ) ) ;
#2858=CARTESIAN_POINT ( 'NONE',  ( 0.000000000000000000, 0.000000000000000000, 0.000000000000000000 ) ) ;
#2963=DIRECTION ( 'NONE',  ( 0.000000000000000000, 0.000000000000000000, 1.000000000000000000 ) ) ;
#3109=PRODUCT_DEFINITION_SHAPE ( 'NONE', 'NONE',  #8624 ) ;
#3142=VERTEX_POINT ( 'NONE', #16099 ) ;
#3155=CARTESIAN_POINT ( 'NONE',  ( 0.000000000000000000, -0.5999999999999789946, -3.054668707061614086 ) ) ;
#3274=DIRECTION ( 'NONE',  ( 1.134196829589822059E-15, 6.741645191078037727E-32, -1.000000000000000000 ) ) ;
#3379=FACE_OUTER_BOUND ( 'NONE', #16026, .T. ) ;
#3397=CIRCLE ( 'NONE', #11268, 3.113037248396080425 ) ;
#3427=CARTESIAN_POINT ( 'NONE',  ( -5.089746846163173136E-15, 5.495644160703784365E-16, 4.487534009422209813 ) ) ;
#3463=EDGE_LOOP ( 'NONE', ( #15742, #4728, #11787, #887 ) ) ;
#3468=DIRECTION ( 'NONE',  ( 1.000000000000000000, -4.615739097524200579E-16, -1.134196829589820086E-15 ) ) ;
#3501=CARTESIAN_POINT ( 'NONE',  ( 0.000000000000000000, -0.5999999999999894307, -4.749999999999948486 ) ) ;
#3547=ORIENTED_EDGE ( 'NONE', *, *, #5939, .F. ) ;
#3553=CIRCLE ( 'NONE', #12560, 2.499999999999990674 ) ;
#3613=PLANE ( 'NONE',  #13407 ) ;
#3617=CIRCLE ( 'NONE', #14510, 3.113037248396080425 ) ;
#3645=CARTESIAN_POINT ( 'NONE',  ( 0.1419055191998256638, 0.6000000000000126343, -3.724211676661837167 ) ) ;
#3695=CARTESIAN_POINT ( 'NONE',  ( 0.000000000000000000, 0.6000000000000137446, 3.054668707061600319 ) ) ;
#3806=CARTESIAN_POINT ( 'NONE',  ( 0.1429064800269952973, 0.6000000000000133005, 3.726828488909540216 ) ) ;
#3895=EDGE_CURVE ( 'NONE', #547, #19657, #1108, .T. ) ;
#3915=VERTEX_POINT ( 'NONE', #12049 ) ;
#3961=DIRECTION ( 'NONE',  ( 4.615739097524196635E-16, -1.000000000000000000, -2.220446049250317025E-16 ) ) ;
#4054=( NAMED_UNIT ( * ) PLANE_ANGLE_UNIT ( ) SI_UNIT ( $, .RADIAN. ) );
#4137=UNCERTAINTY_MEASURE_WITH_UNIT (LENGTH_MEASURE( 1.000000000000000082E-05 ), #21562, 'distance_accuracy_value', 'NONE');
#4254=ORIENTED_EDGE ( 'NONE', *, *, #4622, .F. ) ;
#4520=CONICAL_SURFACE ( 'NONE', #13908, 4.487534009422209813, 0.08726646259971666819 ) ;
#4527=CARTESIAN_POINT ( 'NONE',  ( 1.199999999999992628, -0.5999999999999963141, 4.543283425070391068 ) ) ;
#4571=EDGE_LOOP ( 'NONE', ( #20283, #21646, #6979, #16063 ) ) ;
#4622=EDGE_CURVE ( 'NONE', #3142, #12159, #13354, .T. ) ;
#4641=EDGE_CURVE ( 'NONE', #20325, #12512, #12801, .T. ) ;
#4665=ORIENTED_EDGE ( 'NONE', *, *, #5939, .T. ) ;
#4711=DIRECTION ( 'NONE',  ( -1.000000000000000000, 4.615739097524200579E-16, 1.134196829589820086E-15 ) ) ;
#4715=CARTESIAN_POINT ( 'NONE',  ( 0.000000000000000000, 0.6000000000000137446, 3.054668707061600319 ) ) ;
#4728=ORIENTED_EDGE ( 'NONE', *, *, #1907, .T. ) ;
#4796=CIRCLE ( 'NONE', #11176, 2.499999999999990674 ) ;
#4907=EDGE_CURVE ( 'NONE', #12159, #20325, #3617, .T. ) ;
#4943=CARTESIAN_POINT ( 'NONE',  ( 0.000000000000000000, 0.000000000000000000, 0.000000000000000000 ) ) ;
#4957=CARTESIAN_POINT ( 'NONE',  ( 1.500000000000004885, 3.812371101874739144E-16, -3.113037248396080425 ) ) ;
#4963=DIRECTION ( 'NONE',  ( 1.000000000000000000, -4.615739097524200579E-16, -1.134196829589820086E-15 ) ) ;
#5016=VERTEX_POINT ( 'NONE', #15589 ) ;
#5026=DIRECTION ( 'NONE',  ( -1.000000000000000000, 4.615739097524200579E-16, 1.134196829589820086E-15 ) ) ;
#5029=LINE ( 'NONE', #3501, #13471 ) ;
#5241=DIRECTION ( 'NONE',  ( 1.000000000000000000, -4.615739097524200579E-16, -1.134196829589820086E-15 ) ) ;
#5271=DIRECTION ( 'NONE',  ( -1.134196829589822256E-15, -2.220446049250322449E-16, 1.000000000000000000 ) ) ;
#5305=LINE ( 'NONE', #3427, #19852 ) ;
#5306=DIRECTION ( 'NONE',  ( 1.000000000000000000, 0.000000000000000000, 0.000000000000000000 ) ) ;
#5373=DIRECTION ( 'NONE',  ( -1.214306433183769502E-15, -6.741645191078037727E-32, 1.000000000000000000 ) ) ;
#5381=ORIENTED_EDGE ( 'NONE', *, *, #6980, .F. ) ;
#5433=ORIENTED_EDGE ( 'NONE', *, *, #16391, .T. ) ;
#5447=( NAMED_UNIT ( * ) SI_UNIT ( $, .STERADIAN. ) SOLID_ANGLE_UNIT ( ) );
#5492=ORIENTED_EDGE ( 'NONE', *, *, #12669, .F. ) ;
#5510=DIRECTION ( 'NONE',  ( -1.000000000000000000, 4.615739097524200579E-16, 1.134196829589820086E-15 ) ) ;
#5522=AXIS2_PLACEMENT_3D ( 'NONE', #16181, #7267, #10781 ) ;
#5589=ORIENTED_EDGE ( 'NONE', *, *, #2060, .T. ) ;
#5590=CARTESIAN_POINT ( 'NONE',  ( 1.030267906253071075, 0.6000000000000137446, 4.508336184329987617 ) ) ;
#5602=COLOUR_RGB ( '', 0.31764706, 0.68627451, 0.89019608) ;
#5770=CARTESIAN_POINT ( 'NONE',  ( 1.369266385878517678, 0.000000000000000000, 0.000000000000000000 ) ) ;
#5871=ORIENTED_EDGE ( 'NONE', *, *, #16998, .F. ) ;
#5898=FACE_OUTER_BOUND ( 'NONE', #20449, .T. ) ;
#5899=CARTESIAN_POINT ( 'NONE',  ( 1.199999999999992628, 0.000000000000000000, 0.000000000000000000 ) ) ;
#5939=EDGE_CURVE ( 'NONE', #3915, #13552, #21367, .T. ) ;
#6020=CARTESIAN_POINT ( 'NONE',  ( 0.4425134659200216647, -0.5999999999999892086, 4.147378741782005385 ) ) ;
#6214=VERTEX_POINT ( 'NONE', #9995 ) ;
#6260=ADVANCED_FACE ( 'NONE', ( #10793 ), #8219, .T. ) ;
#6279=PLANE ( 'NONE',  #19931 ) ;
#6343=ADVANCED_FACE ( 'NONE', ( #14096 ), #14924, .T. ) ;
#6380=DIRECTION ( 'NONE',  ( -1.387778780781450803E-15, 0.000000000000000000, 1.000000000000000000 ) ) ;
#6382=CARTESIAN_POINT ( 'NONE',  ( 0.000000000000000000, 0.000000000000000000, 0.000000000000000000 ) ) ;
#6387=EDGE_LOOP ( 'NONE', ( #14332, #10250, #18668, #10996 ) ) ;
#6477=PRODUCT ( 'slotted pan head screw_bsi_BS EN ISO 1580 - M5 x 25 - 25N', 'slotted pan head screw_bsi_BS EN ISO 1580 - M5 x 25 - 25N', '', ( #16459 ) ) ;
#6509=FACE_OUTER_BOUND ( 'NONE', #205, .T. ) ;
#6539=VERTEX_POINT ( 'NONE', #1565 ) ;
#6551=CIRCLE ( 'NONE', #15931, 4.582731094065982447 ) ;
#6575=CARTESIAN_POINT ( 'NONE',  ( 0.000000000000000000, 0.6000000000000137446, 4.749999999999990230 ) ) ;
#6616=DIRECTION ( 'NONE',  ( -1.095614826932724588E-15, -6.741645191078037727E-32, 1.000000000000000000 ) ) ;
#6793=CARTESIAN_POINT ( 'NONE',  ( 27.99999999999991473, 2.500000000000009326, 0.000000000000000000 ) ) ;
#6901=CIRCLE ( 'NONE', #23058, 4.582731094065982447 ) ;
#6923=ADVANCED_FACE ( 'NONE', ( #18961 ), #15416, .T. ) ;
#6979=ORIENTED_EDGE ( 'NONE', *, *, #22623, .F. ) ;
#6980=EDGE_CURVE ( 'NONE', #13552, #547, #5305, .T. ) ;
#7102=DIRECTION ( 'NONE',  ( -1.000000000000000000, 4.615739097524201565E-16, 0.000000000000000000 ) ) ;
#7192=DIRECTION ( 'NONE',  ( 0.9961946980917456562, -4.491439815345159091E-16, 0.08715574274765708340 ) ) ;
#7209=CARTESIAN_POINT ( 'NONE',  ( 0.000000000000000000, 0.000000000000000000, 0.000000000000000000 ) ) ;
#7243=ADVANCED_BREP_SHAPE_REPRESENTATION ( '', ( #13034, #22115 ), #14985 ) ;
#7267=DIRECTION ( 'NONE',  ( 1.000000000000000000, -4.615739097524200579E-16, -1.134196829589820086E-15 ) ) ;
#7385=EDGE_CURVE ( 'NONE', #15168, #14019, #21740, .T. ) ;
#7439=CARTESIAN_POINT ( 'NONE',  ( 0.1422498215951156220, -0.5999999999999894307, 3.724967290803227193 ) ) ;
#7590=SURFACE_STYLE_USAGE ( .BOTH. , #16288 ) ;
#7612=DIRECTION ( 'NONE',  ( 1.134196829589822256E-15, 2.220446049250322449E-16, -1.000000000000000000 ) ) ;
#7667=CARTESIAN_POINT ( 'NONE',  ( 1.031902578047550589, -0.5999999999999896527, -4.508672757499345707 ) ) ;
#7773=CARTESIAN_POINT ( 'NONE',  ( 0.4427966827908824676, -0.5999999999999897637, -4.147834322102026405 ) ) ;
#7776=CARTESIAN_POINT ( 'NONE',  ( 5.089746846163173136E-15, 3.025336207442039000E-31, -4.487534009422209813 ) ) ;
#7786=PLANE ( 'NONE',  #10457 ) ;
#7893=CARTESIAN_POINT ( 'NONE',  ( 0.000000000000000000, -0.5999999999999859890, 3.054668707061614086 ) ) ;
#8017=DIRECTION ( 'NONE',  ( 0.9961946980917454342, -4.598174816728386208E-16, -0.08715574274765928997 ) ) ;
#8029=AXIS2_PLACEMENT_3D ( 'NONE', #9383, #3961, #7612 ) ;
#8103=FACE_OUTER_BOUND ( 'NONE', #4571, .T. ) ;
#8175=AXIS2_PLACEMENT_3D ( 'NONE', #2667, #9846, #5373 ) ;
#8185=EDGE_LOOP ( 'NONE', ( #3547, #18912, #18845, #20939, #23207, #1037, #9795, #22726 ) ) ;
#8219=TOROIDAL_SURFACE ( 'NONE', #9670, 3.113037248396092416, 1.500000000000000000 ) ;
#8304=CARTESIAN_POINT ( 'NONE',  ( 1.199999999999992628, 0.6000000000000137446, 4.749999999999990230 ) ) ;
#8366=CARTESIAN_POINT ( 'NONE',  ( -25.39999999999989555, 2.775557561562891351E-14, 6.938893903907228378E-14 ) ) ;
#8384=DIRECTION ( 'NONE',  ( -1.000000000000000000, 4.615739097524200579E-16, 1.134196829589820086E-15 ) ) ;
#8453=CARTESIAN_POINT ( 'NONE',  ( -25.39999999999989910, 2.775557561562891351E-14, 2.500000000000059952 ) ) ;
#8565=DIRECTION ( 'NONE',  ( 1.134196829589822059E-15, 6.741645191078037727E-32, -1.000000000000000000 ) ) ;
#8624=PRODUCT_DEFINITION ( 'UNKNOWN', '', #13895, #13584 ) ;
#8707=CARTESIAN_POINT ( 'NONE',  ( 0.8691381963085855755, 0.6000000000000128564, -4.444516329276114064 ) ) ;
#8763=CARTESIAN_POINT ( 'NONE',  ( 1.369266385878517678, 0.000000000000000000, 0.000000000000000000 ) ) ;
#8810=AXIS2_PLACEMENT_3D ( 'NONE', #17079, #4963, #13688 ) ;
#8893=CARTESIAN_POINT ( 'NONE',  ( 3.000000000000002665, 2.499999999999998668, 2.775557561562891351E-14 ) ) ;
#8915=CARTESIAN_POINT ( 'NONE',  ( 0.000000000000000000, 0.000000000000000000, 0.000000000000000000 ) ) ;
#9037=DIRECTION ( 'NONE',  ( -1.000000000000000000, 4.615739097524200579E-16, -1.134196829589822059E-15 ) ) ;
#9064=ORIENTED_EDGE ( 'NONE', *, *, #22623, .T. ) ;
#9174=CARTESIAN_POINT ( 'NONE',  ( 1.030796516412017860, 0.6000000000000129674, -4.508445023301312027 ) ) ;
#9312=DIRECTION ( 'NONE',  ( 1.000000000000000000, -4.615739097524200579E-16, -1.134196829589820086E-15 ) ) ;
#9340=ORIENTED_EDGE ( 'NONE', *, *, #16103, .F. ) ;
#9341=CARTESIAN_POINT ( 'NONE',  ( 0.4436723136282449964, 0.6000000000000134115, 4.148801034132779897 ) ) ;
#9383=CARTESIAN_POINT ( 'NONE',  ( 1.200000000000006617, -0.5999999999999894307, -4.749999999999948486 ) ) ;
#9432=CARTESIAN_POINT ( 'NONE',  ( 1.199999999999992628, -0.5999999999999963141, 4.543283425070391068 ) ) ;
#9443=ORIENTED_EDGE ( 'NONE', *, *, #4907, .T. ) ;
#9524=DIRECTION ( 'NONE',  ( 1.000000000000000000, -4.615739097524200579E-16, -1.134196829589820086E-15 ) ) ;
#9551=CARTESIAN_POINT ( 'NONE',  ( 0.02857727139927065951, -0.5999999999999898748, -3.398545894033815795 ) ) ;
#9562=AXIS2_PLACEMENT_3D ( 'NONE', #10148, #8384, #6616 ) ;
#9670=AXIS2_PLACEMENT_3D ( 'NONE', #21166, #1514, #14220 ) ;
#9740=MECHANICAL_DESIGN_GEOMETRIC_PRESENTATION_REPRESENTATION('',(#15720),#11588);
#9795=ORIENTED_EDGE ( 'NONE', *, *, #19503, .T. ) ;
#9815=DIRECTION ( 'NONE',  ( -4.615739097524193676E-16, 1.000000000000000000, -4.560992131517923160E-31 ) ) ;
#9846=DIRECTION ( 'NONE',  ( -1.000000000000000000, 4.615739097524200579E-16, 1.134196829589820086E-15 ) ) ;
#9995=CARTESIAN_POINT ( 'NONE',  ( 2.999999999999999556, 9.183364406541944790E-15, -2.500000000000000444 ) ) ;
#10103=DIRECTION ( 'NONE',  ( -1.000000000000000000, 4.615739097524200579E-16, 1.134196829589820086E-15 ) ) ;
#10148=CARTESIAN_POINT ( 'NONE',  ( 3.000000000000002665, 0.000000000000000000, 0.000000000000000000 ) ) ;
#10248=APPLICATION_CONTEXT ( 'automotive_design' ) ;
#10250=ORIENTED_EDGE ( 'NONE', *, *, #2439, .T. ) ;
#10307=VERTEX_POINT ( 'NONE', #757 ) ;
#10347=CARTESIAN_POINT ( 'NONE',  ( 27.99999999999991473, -3.469446951953614189E-15, -2.775557561562891351E-14 ) ) ;
#10423=DIRECTION ( 'NONE',  ( -1.134196829589822059E-15, -6.741645191078037727E-32, 1.000000000000000000 ) ) ;
#10457=AXIS2_PLACEMENT_3D ( 'NONE', #6382, #13434, #22380 ) ;
#10601=SURFACE_STYLE_FILL_AREA ( #19549 ) ;
#10608=CARTESIAN_POINT ( 'NONE',  ( 3.000000000000002665, 0.000000000000000000, 0.000000000000000000 ) ) ;
#10681=DIRECTION ( 'NONE',  ( 1.134196829589819889E-15, -1.111653967262545517E-30, 1.000000000000000000 ) ) ;
#10752=VECTOR ( 'NONE', #2327, 1000.000000000000000 ) ;
#10781=DIRECTION ( 'NONE',  ( 1.134196829589822059E-15, 6.741645191078038822E-32, -1.000000000000000000 ) ) ;
#10793=FACE_OUTER_BOUND ( 'NONE', #22763, .T. ) ;
#10803=DIRECTION ( 'NONE',  ( 1.000000000000000000, -4.615739097524200579E-16, -1.134196829589820086E-15 ) ) ;
#10812=CARTESIAN_POINT ( 'NONE',  ( 0.4414465083558130054, 0.6000000000000127454, -4.146294842461959895 ) ) ;
#10915=CARTESIAN_POINT ( 'NONE',  ( 0.5741843527964847205, 0.6000000000000127454, -4.263785792382347672 ) ) ;
#10950=CARTESIAN_POINT ( 'NONE',  ( 1.499999999999997780, -2.098699259529624113E-31, 3.113037248396080425 ) ) ;
#10996=ORIENTED_EDGE ( 'NONE', *, *, #926, .F. ) ;
#11069=CARTESIAN_POINT ( 'NONE',  ( 0.5724039806123020213, -0.5999999999999899858, -4.262472862582134425 ) ) ;
#11094=CARTESIAN_POINT ( 'NONE',  ( 0.2261952378970901179, 0.6000000000000133005, 3.877637771780682030 ) ) ;
#11112=ORIENTED_EDGE ( 'NONE', *, *, #4907, .F. ) ;
#11147=VERTEX_POINT ( 'NONE', #16987 ) ;
#11176=AXIS2_PLACEMENT_3D ( 'NONE', #10347, #4711, #11881 ) ;
#11268=AXIS2_PLACEMENT_3D ( 'NONE', #2158, #14637, #18179 ) ;
#11301=LINE ( 'NONE', #7776, #20846 ) ;
#11336=ORIENTED_EDGE ( 'NONE', *, *, #18183, .T. ) ;
#11458=( NAMED_UNIT ( * ) PLANE_ANGLE_UNIT ( ) SI_UNIT ( $, .RADIAN. ) );
#11588=( GEOMETRIC_REPRESENTATION_CONTEXT ( 3 ) GLOBAL_UNCERTAINTY_ASSIGNED_CONTEXT ( ( #11687 ) ) GLOBAL_UNIT_ASSIGNED_CONTEXT ( ( #14760, #4054, #2290 ) ) REPRESENTATION_CONTEXT ( 'NONE', 'WORKASPACE' ) );
#11631=AXIS2_PLACEMENT_3D ( 'NONE', #8763, #3468, #19581 ) ;
#11687=UNCERTAINTY_MEASURE_WITH_UNIT (LENGTH_MEASURE( 1.000000000000000082E-05 ), #14760, 'distance_accuracy_value', 'NONE');
#11787=ORIENTED_EDGE ( 'NONE', *, *, #16040, .T. ) ;
#11856=ORIENTED_EDGE ( 'NONE', *, *, #12723, .T. ) ;
#11857=EDGE_CURVE ( 'NONE', #3142, #1999, #6901, .T. ) ;
#11881=DIRECTION ( 'NONE',  ( -1.387778780781450803E-15, 0.000000000000000000, 1.000000000000000000 ) ) ;
#12000=CIRCLE ( 'NONE', #11631, 4.607329295533694413 ) ;
#12031=VECTOR ( 'NONE', #14028, 1000.000000000000000 ) ;
#12049=CARTESIAN_POINT ( 'NONE',  ( 1.369266385878512349, -1.008369684239886283E-15, -4.607329295533711289 ) ) ;
#12159=VERTEX_POINT ( 'NONE', #3155 ) ;
#12184=CIRCLE ( 'NONE', #9562, 4.749999999999981348 ) ;
#12202=DIRECTION ( 'NONE',  ( -1.387778780781450803E-15, 0.000000000000000000, 1.000000000000000000 ) ) ;
#12308=DIRECTION ( 'NONE',  ( 1.000000000000000000, -4.615739097524200579E-16, 1.134196829589822059E-15 ) ) ;
#12410=DIRECTION ( 'NONE',  ( -1.000000000000000000, 4.615739097524200579E-16, -1.134196829589822059E-15 ) ) ;
#12512=VERTEX_POINT ( 'NONE', #4527 ) ;
#12547=FACE_OUTER_BOUND ( 'NONE', #21614, .T. ) ;
#12560=AXIS2_PLACEMENT_3D ( 'NONE', #10608, #1897, #17802 ) ;
#12597=ORIENTED_EDGE ( 'NONE', *, *, #1907, .F. ) ;
#12669=EDGE_CURVE ( 'NONE', #1999, #10307, #6551, .T. ) ;
#12723=EDGE_CURVE ( 'NONE', #2067, #19898, #16290, .T. ) ;
#12801=B_SPLINE_CURVE_WITH_KNOTS ( 'NONE', 3,
 ( #7893, #15054, #494, #7439, #14947, #6020, #13191, #14607, #12960, #9432 ),
 .UNSPECIFIED., .F., .F.,
 ( 4, 2, 2, 2, 4 ),
 ( 0.001941010781631091840, 0.002456031491763887437, 0.002971052201896682600, 0.003486072912029479064, 0.004001093622162275529 ),
 .UNSPECIFIED. ) ;
#12912=FACE_OUTER_BOUND ( 'NONE', #6387, .T. ) ;
#12960=CARTESIAN_POINT ( 'NONE',  ( 1.031246673762468813, -0.5999999999999888756, 4.508537709115514325 ) ) ;
#13026=CONICAL_SURFACE ( 'NONE', #5522, 4.487534009422209813, 0.08726646259971666819 ) ;
#13034=MANIFOLD_SOLID_BREP ( 'Slot', #19334 ) ;
#13046=CARTESIAN_POINT ( 'NONE',  ( 1.199999999999992628, 0.6000000000000103029, 4.543283425070376857 ) ) ;
#13191=CARTESIAN_POINT ( 'NONE',  ( 0.5743220282100064411, -0.5999999999999890976, 4.263778219380819579 ) ) ;
#13220=AXIS2_PLACEMENT_3D ( 'NONE', #4957, #23215, #7102 ) ;
#13230=SURFACE_STYLE_FILL_AREA ( #541 ) ;
#13235=VECTOR ( 'NONE', #17341, 1000.000000000000000 ) ;
#13354=B_SPLINE_CURVE_WITH_KNOTS ( 'NONE', 3,
 ( #20134, #7667, #609, #11069, #7773, #2362, #14713, #9551, #18374, #22015 ),
 .UNSPECIFIED., .F., .F.,
 ( 4, 2, 2, 2, 4 ),
 ( 0.008920163802561163410, 0.009434751658411351383, 0.009949339514261541090, 0.01046392737011172906, 0.01097851522596191877 ),
 .UNSPECIFIED. ) ;
#13407=AXIS2_PLACEMENT_3D ( 'NONE', #6793, #12308, #3274 ) ;
#13434=DIRECTION ( 'NONE',  ( -1.000000000000000000, 4.615739097524200579E-16, -1.134196829589822059E-15 ) ) ;
#13471=VECTOR ( 'NONE', #5271, 1000.000000000000000 ) ;
#13552=VERTEX_POINT ( 'NONE', #20786 ) ;
#13584=PRODUCT_DEFINITION_CONTEXT ( 'detailed design', #230, 'design' ) ;
#13585=EDGE_CURVE ( 'NONE', #13552, #3915, #12000, .T. ) ;
#13617=ORIENTED_EDGE ( 'NONE', *, *, #64, .F. ) ;
#13684=PRESENTATION_STYLE_ASSIGNMENT (( #1675 ) ) ;
#13688=DIRECTION ( 'NONE',  ( -1.135604581876758782E-15, 6.128431095930851481E-14, 1.000000000000000000 ) ) ;
#13701=DIRECTION ( 'NONE',  ( -1.134196829589822059E-15, -6.741645191078037727E-32, 1.000000000000000000 ) ) ;
#13716=LINE ( 'NONE', #8304, #13235 ) ;
#13724=DIRECTION ( 'NONE',  ( -1.000000000000000000, 4.615739097524200579E-16, 1.134196829589820086E-15 ) ) ;
#13742=EDGE_CURVE ( 'NONE', #19898, #11147, #3397, .T. ) ;
#13790=ORIENTED_EDGE ( 'NONE', *, *, #926, .T. ) ;
#13895=PRODUCT_DEFINITION_FORMATION_WITH_SPECIFIED_SOURCE ( 'ANY', '', #6477, .NOT_KNOWN. ) ;
#13908=AXIS2_PLACEMENT_3D ( 'NONE', #7209, #9312, #18030 ) ;
#13934=ADVANCED_FACE ( 'NONE', ( #6509 ), #6279, .T. ) ;
#14019=VERTEX_POINT ( 'NONE', #21334 ) ;
#14028=DIRECTION ( 'NONE',  ( -1.000000000000000000, 4.615739097524200579E-16, 1.134196829589820086E-15 ) ) ;
#14096=FACE_OUTER_BOUND ( 'NONE', #8185, .T. ) ;
#14102=EDGE_CURVE ( 'NONE', #14019, #6214, #19203, .T. ) ;
#14117=CARTESIAN_POINT ( 'NONE',  ( -3.306986032670239384E-14, 0.6000000000000128564, -3.226721766443178208 ) ) ;
#14156=ADVANCED_FACE ( 'NONE', ( #5898 ), #4520, .T. ) ;
#14220=DIRECTION ( 'NONE',  ( 1.134196829589819889E-15, -1.111653967262545517E-30, 1.000000000000000000 ) ) ;
#14236=CARTESIAN_POINT ( 'NONE',  ( 0.000000000000000000, 0.5999999999999859890, -3.054668707061614086 ) ) ;
#14268=CARTESIAN_POINT ( 'NONE',  ( 2.999999999999997335, -1.384721729257256131E-15, -4.749999999999984901 ) ) ;
#14332=ORIENTED_EDGE ( 'NONE', *, *, #4622, .T. ) ;
#14451=DIRECTION ( 'NONE',  ( -1.134196829589822059E-15, -6.741645191078037727E-32, 1.000000000000000000 ) ) ;
#14453=CARTESIAN_POINT ( 'NONE',  ( 27.99999999999991473, -3.469446951953614189E-15, -2.775557561562891351E-14 ) ) ;
#14510=AXIS2_PLACEMENT_3D ( 'NONE', #8915, #20087, #19965 ) ;
#14515=CARTESIAN_POINT ( 'NONE',  ( 0.8691243128804460039, 0.6000000000000137446, 4.444585127983383899 ) ) ;
#14597=ORIENTED_EDGE ( 'NONE', *, *, #19737, .T. ) ;
#14607=CARTESIAN_POINT ( 'NONE',  ( 0.8678420939694135861, -0.5999999999999889866, 4.443813723662904280 ) ) ;
#14637=DIRECTION ( 'NONE',  ( -1.000000000000000000, 4.615739097524200579E-16, 1.134196829589820086E-15 ) ) ;
#14713=CARTESIAN_POINT ( 'NONE',  ( 0.1425507193225079572, -0.5999999999999897637, -3.725915899842239476 ) ) ;
#14742=CARTESIAN_POINT ( 'NONE',  ( 0.5732283800867107315, 0.6000000000000134115, 4.263122468548279365 ) ) ;
#14760=( LENGTH_UNIT ( ) NAMED_UNIT ( * ) SI_UNIT ( .MILLI., .METRE. ) );
#14924=TOROIDAL_SURFACE ( 'NONE', #15285, 3.113037248396092416, 1.500000000000000000 ) ;
#14947=CARTESIAN_POINT ( 'NONE',  ( 0.2271987153435755802, -0.5999999999999894307, 3.878866322980159431 ) ) ;
#14985=( GEOMETRIC_REPRESENTATION_CONTEXT ( 3 ) GLOBAL_UNCERTAINTY_ASSIGNED_CONTEXT ( ( #884 ) ) GLOBAL_UNIT_ASSIGNED_CONTEXT ( ( #16510, #11458, #20181 ) ) REPRESENTATION_CONTEXT ( 'NONE', 'WORKASPACE' ) );
#15054=CARTESIAN_POINT ( 'NONE',  ( -3.225797924675914696E-14, -0.5999999999999898748, 3.226849613583673282 ) ) ;
#15097=ORIENTED_EDGE ( 'NONE', *, *, #16391, .F. ) ;
#15168=VERTEX_POINT ( 'NONE', #20671 ) ;
#15280=EDGE_LOOP ( 'NONE', ( #5381, #2270, #11336, #747 ) ) ;
#15285=AXIS2_PLACEMENT_3D ( 'NONE', #21409, #5510, #10681 ) ;
#15334=PLANE ( 'NONE',  #21718 ) ;
#15337=ORIENTED_EDGE ( 'NONE', *, *, #3895, .T. ) ;
#15416=CYLINDRICAL_SURFACE ( 'NONE', #22472, 2.499999999999990674 ) ;
#15501=DIRECTION ( 'NONE',  ( -1.387778780781450803E-15, 0.000000000000000000, 1.000000000000000000 ) ) ;
#15509=CIRCLE ( 'NONE', #16628, 4.582731094065982447 ) ;
#15536=DIRECTION ( 'NONE',  ( -1.000000000000000000, 4.615739097524200579E-16, 1.134196829589820086E-15 ) ) ;
#15589=CARTESIAN_POINT ( 'NONE',  ( 1.199999999999992628, 1.384721729257273387E-16, 4.582731094065980670 ) ) ;
#15618=ORIENTED_EDGE ( 'NONE', *, *, #3895, .F. ) ;
#15625=ORIENTED_EDGE ( 'NONE', *, *, #13585, .F. ) ;
#15720=STYLED_ITEM ( 'NONE', ( #21720 ), #7243 ) ;
#15742=ORIENTED_EDGE ( 'NONE', *, *, #14102, .F. ) ;
#15775=SURFACE_SIDE_STYLE ('',( #10601 ) ) ;
#15823=EDGE_CURVE ( 'NONE', #3915, #1999, #445, .T. ) ;
#15846=DIRECTION ( 'NONE',  ( -1.000000000000000000, 4.615739097524200579E-16, 1.134196829589820086E-15 ) ) ;
#15931=AXIS2_PLACEMENT_3D ( 'NONE', #17458, #5241, #19577 ) ;
#16026=EDGE_LOOP ( 'NONE', ( #13617, #15618 ) ) ;
#16040=EDGE_CURVE ( 'NONE', #15168, #6539, #1504, .T. ) ;
#16063=ORIENTED_EDGE ( 'NONE', *, *, #16040, .F. ) ;
#16099=CARTESIAN_POINT ( 'NONE',  ( 1.200000000000006617, -0.5999999999999963141, -4.543283425070376857 ) ) ;
#16103=EDGE_CURVE ( 'NONE', #19898, #11147, #20819, .T. ) ;
#16153=CARTESIAN_POINT ( 'NONE',  ( 0.02842916987967946188, 0.6000000000000131894, 3.398229573760024991 ) ) ;
#16165=FACE_BOUND ( 'NONE', #18560, .T. ) ;
#16181=CARTESIAN_POINT ( 'NONE',  ( 0.000000000000000000, 0.000000000000000000, 0.000000000000000000 ) ) ;
#16210=CARTESIAN_POINT ( 'NONE',  ( 0.02893550784256185282, 0.6000000000000127454, -3.399425482353690242 ) ) ;
#16221=VECTOR ( 'NONE', #8565, 1000.000000000000000 ) ;
#16288=SURFACE_SIDE_STYLE ('',( #13230 ) ) ;
#16290=B_SPLINE_CURVE_WITH_KNOTS ( 'NONE', 3,
 ( #407, #5590, #14515, #14742, #9341, #11094, #3806, #16153, #18278, #3695 ),
 .UNSPECIFIED., .F., .F.,
 ( 4, 2, 2, 2, 4 ),
 ( 0.005493704601871788815, 0.006008885122700079531, 0.006524065643528370248, 0.007039246164356660965, 0.007554426685184951681 ),
 .UNSPECIFIED. ) ;
#16354=( NAMED_UNIT ( * ) PLANE_ANGLE_UNIT ( ) SI_UNIT ( $, .RADIAN. ) );
#16357=DIRECTION ( 'NONE',  ( -1.135604581876758782E-15, -6.741645191078037727E-32, 1.000000000000000000 ) ) ;
#16391=EDGE_CURVE ( 'NONE', #2067, #10307, #13716, .T. ) ;
#16459=PRODUCT_CONTEXT ( 'NONE', #10248, 'mechanical' ) ;
#16476=AXIS2_PLACEMENT_3D ( 'NONE', #18781, #13724, #17114 ) ;
#16510=( LENGTH_UNIT ( ) NAMED_UNIT ( * ) SI_UNIT ( .MILLI., .METRE. ) );
#16628=AXIS2_PLACEMENT_3D ( 'NONE', #5899, #728, #16357 ) ;
#16947=ORIENTED_EDGE ( 'NONE', *, *, #16103, .T. ) ;
#16987=CARTESIAN_POINT ( 'NONE',  ( 0.000000000000000000, 0.5999999999999859890, -3.054668707061614086 ) ) ;
#16998=EDGE_CURVE ( 'NONE', #5016, #12512, #15509, .T. ) ;
#17079=CARTESIAN_POINT ( 'NONE',  ( 1.199999999999992628, 0.000000000000000000, 0.000000000000000000 ) ) ;
#17103=EDGE_LOOP ( 'NONE', ( #13790, #5871, #23153, #5433, #5492, #2496 ) ) ;
#17114=DIRECTION ( 'NONE',  ( -1.095614826932724588E-15, -6.741645191078037727E-32, 1.000000000000000000 ) ) ;
#17198=DIRECTION ( 'NONE',  ( -1.000000000000000000, 4.615739097524200579E-16, -1.134196829589822059E-15 ) ) ;
#17341=DIRECTION ( 'NONE',  ( 1.134196829589822059E-15, 6.741645191078037727E-32, -1.000000000000000000 ) ) ;
#17458=CARTESIAN_POINT ( 'NONE',  ( 1.199999999999992628, 0.000000000000000000, 0.000000000000000000 ) ) ;
#17501=CARTESIAN_POINT ( 'NONE',  ( 1.200000000000006617, 0.5999999999999998668, -4.749999999999948486 ) ) ;
#17546=CARTESIAN_POINT ( 'NONE',  ( -25.39999999999989200, 2.806173731541575138E-14, -2.499999999999920952 ) ) ;
#17785=ORIENTED_EDGE ( 'NONE', *, *, #16998, .T. ) ;
#17802=DIRECTION ( 'NONE',  ( -1.214306433183769502E-15, -6.741645191078037727E-32, 1.000000000000000000 ) ) ;
#17860=AXIS2_PLACEMENT_3D ( 'NONE', #22571, #10103, #15501 ) ;
#17902=AXIS2_PLACEMENT_3D ( 'NONE', #8893, #12410, #10423 ) ;
#18004=CARTESIAN_POINT ( 'NONE',  ( 0.2265654810057098067, 0.6000000000000128564, -3.877828006771827596 ) ) ;
#18018=EDGE_CURVE ( 'NONE', #13552, #5016, #21949, .T. ) ;
#18030=DIRECTION ( 'NONE',  ( 1.134196829589822059E-15, 6.741645191078038822E-32, -1.000000000000000000 ) ) ;
#18179=DIRECTION ( 'NONE',  ( -1.134196829589822059E-15, -6.741645191078037727E-32, 1.000000000000000000 ) ) ;
#18183=EDGE_CURVE ( 'NONE', #3915, #19657, #11301, .T. ) ;
#18278=CARTESIAN_POINT ( 'NONE',  ( -8.658472430787128582E-13, 0.6000000000000130784, 3.228722604634005844 ) ) ;
#18374=CARTESIAN_POINT ( 'NONE',  ( -3.529586291208667935E-15, -0.5999999999999897637, -3.228048788193013774 ) ) ;
#18446=LINE ( 'NONE', #2447, #10752 ) ;
#18500=ORIENTED_EDGE ( 'NONE', *, *, #7385, .F. ) ;
#18560=EDGE_LOOP ( 'NONE', ( #9064, #14597 ) ) ;
#18668=ORIENTED_EDGE ( 'NONE', *, *, #4641, .T. ) ;
#18781=CARTESIAN_POINT ( 'NONE',  ( 3.000000000000002665, 0.000000000000000000, 0.000000000000000000 ) ) ;
#18845=ORIENTED_EDGE ( 'NONE', *, *, #12669, .T. ) ;
#18912=ORIENTED_EDGE ( 'NONE', *, *, #15823, .T. ) ;
#18961=FACE_OUTER_BOUND ( 'NONE', #3463, .T. ) ;
#19080=ADVANCED_FACE ( 'NONE', ( #12912 ), #20090, .F. ) ;
#19107=AXIS2_PLACEMENT_3D ( 'NONE', #14453, #15846, #12202 ) ;
#19153=CARTESIAN_POINT ( 'NONE',  ( 0.000000000000000000, -0.5999999999999859890, 3.054668707061614086 ) ) ;
#19203=LINE ( 'NONE', #17546, #12031 ) ;
#19242=VECTOR ( 'NONE', #5026, 1000.000000000000000 ) ;
#19334=CLOSED_SHELL ( 'NONE', ( #6343, #14156, #20188, #13934, #6923, #1207, #23175, #1198, #21663, #6260, #22807, #19080, #21319 ) ) ;
#19503=EDGE_CURVE ( 'NONE', #2067, #5016, #20466, .T. ) ;
#19549=FILL_AREA_STYLE ('',( #1438 ) ) ;
#19557=DIRECTION ( 'NONE',  ( 1.000000000000000000, -4.615739097524200579E-16, 0.000000000000000000 ) ) ;
#19577=DIRECTION ( 'NONE',  ( -1.135604581876758782E-15, 1.065814103640148386E-14, 1.000000000000000000 ) ) ;
#19581=DIRECTION ( 'NONE',  ( -1.129541670263356189E-15, -6.741645191078037727E-32, 1.000000000000000000 ) ) ;
#19622=FACE_OUTER_BOUND ( 'NONE', #17103, .T. ) ;
#19644=CARTESIAN_POINT ( 'NONE',  ( 1.199999999999992628, 6.996948694958265185E-16, -4.582731094065978894 ) ) ;
#19657=VERTEX_POINT ( 'NONE', #14268 ) ;
#19737=EDGE_CURVE ( 'NONE', #6214, #6539, #3553, .T. ) ;
#19756=ORIENTED_EDGE ( 'NONE', *, *, #15823, .F. ) ;
#19852=VECTOR ( 'NONE', #7192, 1000.000000000000000 ) ;
#19898=VERTEX_POINT ( 'NONE', #4715 ) ;
#19931=AXIS2_PLACEMENT_3D ( 'NONE', #2858, #17198, #869 ) ;
#19965=DIRECTION ( 'NONE',  ( -1.134196829589822059E-15, -6.741645191078037727E-32, 1.000000000000000000 ) ) ;
#20003=ORIENTED_EDGE ( 'NONE', *, *, #4641, .F. ) ;
#20063=AXIS2_PLACEMENT_3D ( 'NONE', #10950, #21573, #19557 ) ;
#20087=DIRECTION ( 'NONE',  ( -1.000000000000000000, 4.615739097524200579E-16, 1.134196829589820086E-15 ) ) ;
#20090=PLANE ( 'NONE',  #8029 ) ;
#20119=SHAPE_DEFINITION_REPRESENTATION ( #3109, #22944 ) ;
#20134=CARTESIAN_POINT ( 'NONE',  ( 1.200000000000006617, -0.5999999999999963141, -4.543283425070376857 ) ) ;
#20149=AXIS2_PLACEMENT_3D ( 'NONE', #17501, #9037, #14451 ) ;
#20181=( NAMED_UNIT ( * ) SI_UNIT ( $, .STERADIAN. ) SOLID_ANGLE_UNIT ( ) );
#20187=ORIENTED_EDGE ( 'NONE', *, *, #13742, .T. ) ;
#20188=ADVANCED_FACE ( 'NONE', ( #8103 ), #20579, .T. ) ;
#20197=B_SPLINE_CURVE_WITH_KNOTS ( 'NONE', 3,
 ( #14236, #14117, #16210, #3645, #18004, #10812, #10915, #8707, #9174, #1867 ),
 .UNSPECIFIED., .F., .F.,
 ( 4, 2, 2, 2, 4 ),
 ( 0.008003515366661734937, 0.008517983447693508806, 0.009032451528725282675, 0.009546919609757058278, 0.01006138769078883388 ),
 .UNSPECIFIED. ) ;
#20283=ORIENTED_EDGE ( 'NONE', *, *, #7385, .T. ) ;
#20325=VERTEX_POINT ( 'NONE', #19153 ) ;
#20346=DIRECTION ( 'NONE',  ( -1.129541670263356189E-15, -6.741645191078037727E-32, 1.000000000000000000 ) ) ;
#20409=FACE_OUTER_BOUND ( 'NONE', #22302, .T. ) ;
#20449=EDGE_LOOP ( 'NONE', ( #4665, #2146, #15337, #22383 ) ) ;
#20466=CIRCLE ( 'NONE', #8810, 4.582731094065982447 ) ;
#20579=CYLINDRICAL_SURFACE ( 'NONE', #17860, 2.499999999999990674 ) ;
#20671=CARTESIAN_POINT ( 'NONE',  ( 27.99999999999991118, -3.469446951953614189E-15, 2.499999999999962697 ) ) ;
#20740=ORIENTED_EDGE ( 'NONE', *, *, #18018, .T. ) ;
#20786=CARTESIAN_POINT ( 'NONE',  ( 1.369266385878522785, -4.353985157227390831E-16, 4.607329295533711289 ) ) ;
#20819=LINE ( 'NONE', #6575, #16221 ) ;
#20846=VECTOR ( 'NONE', #8017, 1000.000000000000000 ) ;
#20939=ORIENTED_EDGE ( 'NONE', *, *, #2060, .F. ) ;
#21166=CARTESIAN_POINT ( 'NONE',  ( 1.500000000000001332, 0.000000000000000000, 0.000000000000000000 ) ) ;
#21319=ADVANCED_FACE ( 'NONE', ( #19622 ), #1737, .T. ) ;
#21334=CARTESIAN_POINT ( 'NONE',  ( 27.99999999999991118, 9.183364406542126228E-15, -2.500000000000028422 ) ) ;
#21337=CIRCLE ( 'NONE', #8175, 2.499999999999990674 ) ;
#21367=CIRCLE ( 'NONE', #702, 4.607329295533694413 ) ;
#21409=CARTESIAN_POINT ( 'NONE',  ( 1.500000000000001332, 0.000000000000000000, 0.000000000000000000 ) ) ;
#21562=( LENGTH_UNIT ( ) NAMED_UNIT ( * ) SI_UNIT ( .MILLI., .METRE. ) );
#21573=DIRECTION ( 'NONE',  ( -4.615739097524200579E-16, -1.000000000000000000, -5.909321169733538150E-31 ) ) ;
#21614=EDGE_LOOP ( 'NONE', ( #18500, #12597 ) ) ;
#21646=ORIENTED_EDGE ( 'NONE', *, *, #14102, .T. ) ;
#21663=ADVANCED_FACE ( 'NONE', ( #3379, #16165 ), #83, .F. ) ;
#21718=AXIS2_PLACEMENT_3D ( 'NONE', #1121, #9815, #13701 ) ;
#21720=PRESENTATION_STYLE_ASSIGNMENT (( #7590 ) ) ;
#21740=CIRCLE ( 'NONE', #19107, 2.499999999999990674 ) ;
#21949=CIRCLE ( 'NONE', #20063, 1.500000000000000000 ) ;
#22015=CARTESIAN_POINT ( 'NONE',  ( 0.000000000000000000, -0.5999999999999789946, -3.054668707061614086 ) ) ;
#22115=AXIS2_PLACEMENT_3D ( 'NONE', #4943, #2963, #5306 ) ;
#22288=EDGE_LOOP ( 'NONE', ( #23238, #9443 ) ) ;
#22302=EDGE_LOOP ( 'NONE', ( #5589, #15097, #11856, #16947 ) ) ;
#22380=DIRECTION ( 'NONE',  ( -1.134196829589822059E-15, -6.741645191078037727E-32, 1.000000000000000000 ) ) ;
#22383=ORIENTED_EDGE ( 'NONE', *, *, #18183, .F. ) ;
#22472=AXIS2_PLACEMENT_3D ( 'NONE', #8366, #15536, #6380 ) ;
#22495=FACE_OUTER_BOUND ( 'NONE', #22288, .T. ) ;
#22571=CARTESIAN_POINT ( 'NONE',  ( -25.39999999999989555, 2.775557561562891351E-14, 6.938893903907228378E-14 ) ) ;
#22623=EDGE_CURVE ( 'NONE', #6539, #6214, #21337, .T. ) ;
#22693=MECHANICAL_DESIGN_GEOMETRIC_PRESENTATION_REPRESENTATION('',(#1640),#140);
#22726=ORIENTED_EDGE ( 'NONE', *, *, #18018, .F. ) ;
#22763=EDGE_LOOP ( 'NONE', ( #19756, #15625, #20740, #17785, #20003, #11112, #4254, #509 ) ) ;
#22807=ADVANCED_FACE ( 'NONE', ( #20409 ), #15334, .F. ) ;
#22944=SHAPE_REPRESENTATION ( 'slotted pan head screw_bsi_BS EN ISO 1580 - M5 x 25 - 25N', ( #22115 ), #14985 ) ;
#22945=CARTESIAN_POINT ( 'NONE',  ( 1.199999999999992628, 0.000000000000000000, 0.000000000000000000 ) ) ;
#23058=AXIS2_PLACEMENT_3D ( 'NONE', #22945, #10803, #1745 ) ;
#23069=CARTESIAN_POINT ( 'NONE',  ( 3.000000000000008438, -8.030144996622774890E-16, 4.749999999999979572 ) ) ;
#23153=ORIENTED_EDGE ( 'NONE', *, *, #19503, .F. ) ;
#23175=ADVANCED_FACE ( 'NONE', ( #22495 ), #7786, .T. ) ;
#23207=ORIENTED_EDGE ( 'NONE', *, *, #13742, .F. ) ;
#23215=DIRECTION ( 'NONE',  ( 4.615739097524201565E-16, 1.000000000000000000, 1.224646799147356905E-16 ) ) ;
#23238=ORIENTED_EDGE ( 'NONE', *, *, #2439, .F. ) ;
ENDSEC;
END-ISO-10303-21;
